ISO-10303-21;
HEADER;
/* Generated by software containing ST-Developer
 * from STEP Tools, Inc. (www.steptools.com) 
 */

FILE_DESCRIPTION(
/* description */ ('Shaft runout checking stand'),
/* implementation_level */ '2;1');

FILE_NAME(
/* name */ 'M5x14 Cap Screw.step',
/* time_stamp */ '2026-11-02T21:12:33-08:00',
/* author */ (''),
/* organization */ (''),
/* preprocessor_version */ 'ST-DEVELOPER v20.2',
/* originating_system */ 'Autodesk Translation Framework v15.17.0.0',
/* authorisation */ '');

FILE_SCHEMA (('AUTOMOTIVE_DESIGN { 1 0 10303 214 3 1 1 }'));
ENDSEC;

DATA;
#10=MECHANICAL_DESIGN_GEOMETRIC_PRESENTATION_REPRESENTATION('',(#487),#11748);
#355=ORIENTED_CLOSED_SHELL('',*,#6232,.F.);
#358=BREP_WITH_VOIDS('Body1',#6233,(#355));
#366=CONICAL_SURFACE('',#7140,0.4,0.785398163397448);
#367=CONICAL_SURFACE('',#7144,0.41,0.785398163397448);
#368=CONICAL_SURFACE('',#7148,0.26,0.463647609000806);
#401=SHAPE_REPRESENTATION_RELATIONSHIP('SRR','None',#11950,#444);
#444=ADVANCED_BREP_SHAPE_REPRESENTATION('',(#358),#11726);
#487=STYLED_ITEM('',(#12172),#358);
#640=FACE_BOUND('',#1728,.T.);
#808=CIRCLE('',#7137,0.24505);
#809=CIRCLE('',#7139,0.375);
#810=CIRCLE('',#7141,0.425);
#811=CIRCLE('',#7143,0.425);
#812=CIRCLE('',#7145,0.395);
#813=CIRCLE('',#7147,0.27);
#814=CIRCLE('',#7149,0.24505);
#1001=CYLINDRICAL_SURFACE('',#7142,0.425);
#1002=CYLINDRICAL_SURFACE('',#7150,0.24505);
#1268=FACE_OUTER_BOUND('',#1714,.T.);
#1269=FACE_OUTER_BOUND('',#1715,.T.);
#1270=FACE_OUTER_BOUND('',#1716,.T.);
#1271=FACE_OUTER_BOUND('',#1717,.T.);
#1272=FACE_OUTER_BOUND('',#1718,.T.);
#1273=FACE_OUTER_BOUND('',#1719,.T.);
#1274=FACE_OUTER_BOUND('',#1720,.T.);
#1275=FACE_OUTER_BOUND('',#1721,.T.);
#1276=FACE_OUTER_BOUND('',#1722,.T.);
#1277=FACE_OUTER_BOUND('',#1723,.T.);
#1278=FACE_OUTER_BOUND('',#1724,.T.);
#1279=FACE_OUTER_BOUND('',#1725,.T.);
#1280=FACE_OUTER_BOUND('',#1726,.T.);
#1281=FACE_OUTER_BOUND('',#1727,.T.);
#1282=FACE_OUTER_BOUND('',#1729,.T.);
#1283=FACE_OUTER_BOUND('',#1730,.T.);
#1714=EDGE_LOOP('',(#5082,#5083,#5084,#5085));
#1715=EDGE_LOOP('',(#5086,#5087,#5088,#5089));
#1716=EDGE_LOOP('',(#5090,#5091,#5092,#5093));
#1717=EDGE_LOOP('',(#5094,#5095,#5096,#5097));
#1718=EDGE_LOOP('',(#5098,#5099,#5100,#5101));
#1719=EDGE_LOOP('',(#5102,#5103,#5104,#5105));
#1720=EDGE_LOOP('',(#5106,#5107,#5108,#5109,#5110,#5111));
#1721=EDGE_LOOP('',(#5112,#5113,#5114,#5115,#5116,#5117));
#1722=EDGE_LOOP('',(#5118));
#1723=EDGE_LOOP('',(#5119));
#1724=EDGE_LOOP('',(#5120,#5121,#5122,#5123));
#1725=EDGE_LOOP('',(#5124,#5125,#5126,#5127));
#1726=EDGE_LOOP('',(#5128,#5129,#5130,#5131));
#1727=EDGE_LOOP('',(#5132));
#1728=EDGE_LOOP('',(#5133));
#1729=EDGE_LOOP('',(#5134,#5135,#5136,#5137));
#1730=EDGE_LOOP('',(#5138,#5139,#5140,#5141));
#2245=LINE('',#10561,#2712);
#2246=LINE('',#10563,#2713);
#2247=LINE('',#10565,#2714);
#2248=LINE('',#10566,#2715);
#2249=LINE('',#10569,#2716);
#2250=LINE('',#10571,#2717);
#2251=LINE('',#10572,#2718);
#2252=LINE('',#10575,#2719);
#2253=LINE('',#10577,#2720);
#2254=LINE('',#10578,#2721);
#2255=LINE('',#10581,#2722);
#2256=LINE('',#10583,#2723);
#2257=LINE('',#10584,#2724);
#2258=LINE('',#10587,#2725);
#2259=LINE('',#10589,#2726);
#2260=LINE('',#10590,#2727);
#2261=LINE('',#10592,#2728);
#2262=LINE('',#10593,#2729);
#2263=LINE('',#10605,#2730);
#2264=LINE('',#10609,#2731);
#2265=LINE('',#10613,#2732);
#2266=LINE('',#10620,#2733);
#2267=LINE('',#10622,#2734);
#2712=VECTOR('',#8642,1.);
#2713=VECTOR('',#8643,1.);
#2714=VECTOR('',#8644,1.);
#2715=VECTOR('',#8645,1.);
#2716=VECTOR('',#8648,1.);
#2717=VECTOR('',#8649,1.);
#2718=VECTOR('',#8650,1.);
#2719=VECTOR('',#8653,1.);
#2720=VECTOR('',#8654,1.);
#2721=VECTOR('',#8655,1.);
#2722=VECTOR('',#8658,1.);
#2723=VECTOR('',#8659,1.);
#2724=VECTOR('',#8660,1.);
#2725=VECTOR('',#8663,1.);
#2726=VECTOR('',#8664,1.);
#2727=VECTOR('',#8665,1.);
#2728=VECTOR('',#8668,1.);
#2729=VECTOR('',#8669,1.);
#2730=VECTOR('',#8686,0.4);
#2731=VECTOR('',#8691,0.425);
#2732=VECTOR('',#8696,0.41);
#2733=VECTOR('',#8705,0.26);
#2734=VECTOR('',#8708,0.25);
#3148=VERTEX_POINT('',#10559);
#3149=VERTEX_POINT('',#10560);
#3150=VERTEX_POINT('',#10562);
#3151=VERTEX_POINT('',#10564);
#3152=VERTEX_POINT('',#10568);
#3153=VERTEX_POINT('',#10570);
#3154=VERTEX_POINT('',#10574);
#3155=VERTEX_POINT('',#10576);
#3156=VERTEX_POINT('',#10580);
#3157=VERTEX_POINT('',#10582);
#3158=VERTEX_POINT('',#10586);
#3159=VERTEX_POINT('',#10588);
#3160=VERTEX_POINT('',#10597);
#3161=VERTEX_POINT('',#10600);
#3162=VERTEX_POINT('',#10603);
#3163=VERTEX_POINT('',#10607);
#3164=VERTEX_POINT('',#10611);
#3165=VERTEX_POINT('',#10615);
#3166=VERTEX_POINT('',#10618);
#3827=EDGE_CURVE('',#3148,#3149,#2245,.T.);
#3828=EDGE_CURVE('',#3149,#3150,#2246,.T.);
#3829=EDGE_CURVE('',#3150,#3151,#2247,.T.);
#3830=EDGE_CURVE('',#3148,#3151,#2248,.T.);
#3831=EDGE_CURVE('',#3149,#3152,#2249,.T.);
#3832=EDGE_CURVE('',#3152,#3153,#2250,.T.);
#3833=EDGE_CURVE('',#3153,#3150,#2251,.T.);
#3834=EDGE_CURVE('',#3152,#3154,#2252,.T.);
#3835=EDGE_CURVE('',#3154,#3155,#2253,.T.);
#3836=EDGE_CURVE('',#3155,#3153,#2254,.T.);
#3837=EDGE_CURVE('',#3154,#3156,#2255,.T.);
#3838=EDGE_CURVE('',#3156,#3157,#2256,.T.);
#3839=EDGE_CURVE('',#3157,#3155,#2257,.T.);
#3840=EDGE_CURVE('',#3156,#3158,#2258,.T.);
#3841=EDGE_CURVE('',#3158,#3159,#2259,.T.);
#3842=EDGE_CURVE('',#3159,#3157,#2260,.T.);
#3843=EDGE_CURVE('',#3158,#3148,#2261,.T.);
#3844=EDGE_CURVE('',#3151,#3159,#2262,.T.);
#3845=EDGE_CURVE('',#3160,#3160,#808,.T.);
#3846=EDGE_CURVE('',#3161,#3161,#809,.T.);
#3847=EDGE_CURVE('',#3162,#3162,#810,.T.);
#3848=EDGE_CURVE('',#3162,#3161,#2263,.T.);
#3849=EDGE_CURVE('',#3163,#3163,#811,.T.);
#3850=EDGE_CURVE('',#3163,#3162,#2264,.T.);
#3851=EDGE_CURVE('',#3164,#3164,#812,.T.);
#3852=EDGE_CURVE('',#3164,#3163,#2265,.T.);
#3853=EDGE_CURVE('',#3165,#3165,#813,.T.);
#3854=EDGE_CURVE('',#3166,#3166,#814,.F.);
#3855=EDGE_CURVE('',#3166,#3165,#2266,.T.);
#3856=EDGE_CURVE('',#3160,#3166,#2267,.T.);
#5082=ORIENTED_EDGE('',*,*,#3827,.T.);
#5083=ORIENTED_EDGE('',*,*,#3828,.T.);
#5084=ORIENTED_EDGE('',*,*,#3829,.T.);
#5085=ORIENTED_EDGE('',*,*,#3830,.F.);
#5086=ORIENTED_EDGE('',*,*,#3831,.T.);
#5087=ORIENTED_EDGE('',*,*,#3832,.T.);
#5088=ORIENTED_EDGE('',*,*,#3833,.T.);
#5089=ORIENTED_EDGE('',*,*,#3828,.F.);
#5090=ORIENTED_EDGE('',*,*,#3834,.T.);
#5091=ORIENTED_EDGE('',*,*,#3835,.T.);
#5092=ORIENTED_EDGE('',*,*,#3836,.T.);
#5093=ORIENTED_EDGE('',*,*,#3832,.F.);
#5094=ORIENTED_EDGE('',*,*,#3837,.T.);
#5095=ORIENTED_EDGE('',*,*,#3838,.T.);
#5096=ORIENTED_EDGE('',*,*,#3839,.T.);
#5097=ORIENTED_EDGE('',*,*,#3835,.F.);
#5098=ORIENTED_EDGE('',*,*,#3840,.T.);
#5099=ORIENTED_EDGE('',*,*,#3841,.T.);
#5100=ORIENTED_EDGE('',*,*,#3842,.T.);
#5101=ORIENTED_EDGE('',*,*,#3838,.F.);
#5102=ORIENTED_EDGE('',*,*,#3843,.T.);
#5103=ORIENTED_EDGE('',*,*,#3830,.T.);
#5104=ORIENTED_EDGE('',*,*,#3844,.T.);
#5105=ORIENTED_EDGE('',*,*,#3841,.F.);
#5106=ORIENTED_EDGE('',*,*,#3843,.F.);
#5107=ORIENTED_EDGE('',*,*,#3840,.F.);
#5108=ORIENTED_EDGE('',*,*,#3837,.F.);
#5109=ORIENTED_EDGE('',*,*,#3834,.F.);
#5110=ORIENTED_EDGE('',*,*,#3831,.F.);
#5111=ORIENTED_EDGE('',*,*,#3827,.F.);
#5112=ORIENTED_EDGE('',*,*,#3844,.F.);
#5113=ORIENTED_EDGE('',*,*,#3829,.F.);
#5114=ORIENTED_EDGE('',*,*,#3833,.F.);
#5115=ORIENTED_EDGE('',*,*,#3836,.F.);
#5116=ORIENTED_EDGE('',*,*,#3839,.F.);
#5117=ORIENTED_EDGE('',*,*,#3842,.F.);
#5118=ORIENTED_EDGE('',*,*,#3845,.F.);
#5119=ORIENTED_EDGE('',*,*,#3846,.F.);
#5120=ORIENTED_EDGE('',*,*,#3847,.F.);
#5121=ORIENTED_EDGE('',*,*,#3848,.T.);
#5122=ORIENTED_EDGE('',*,*,#3846,.T.);
#5123=ORIENTED_EDGE('',*,*,#3848,.F.);
#5124=ORIENTED_EDGE('',*,*,#3849,.F.);
#5125=ORIENTED_EDGE('',*,*,#3850,.T.);
#5126=ORIENTED_EDGE('',*,*,#3847,.T.);
#5127=ORIENTED_EDGE('',*,*,#3850,.F.);
#5128=ORIENTED_EDGE('',*,*,#3851,.F.);
#5129=ORIENTED_EDGE('',*,*,#3852,.T.);
#5130=ORIENTED_EDGE('',*,*,#3849,.T.);
#5131=ORIENTED_EDGE('',*,*,#3852,.F.);
#5132=ORIENTED_EDGE('',*,*,#3851,.T.);
#5133=ORIENTED_EDGE('',*,*,#3853,.F.);
#5134=ORIENTED_EDGE('',*,*,#3854,.F.);
#5135=ORIENTED_EDGE('',*,*,#3855,.T.);
#5136=ORIENTED_EDGE('',*,*,#3853,.T.);
#5137=ORIENTED_EDGE('',*,*,#3855,.F.);
#5138=ORIENTED_EDGE('',*,*,#3845,.T.);
#5139=ORIENTED_EDGE('',*,*,#3856,.T.);
#5140=ORIENTED_EDGE('',*,*,#3854,.T.);
#5141=ORIENTED_EDGE('',*,*,#3856,.F.);
#5764=PLANE('',#7128);
#5765=PLANE('',#7129);
#5766=PLANE('',#7130);
#5767=PLANE('',#7131);
#5768=PLANE('',#7132);
#5769=PLANE('',#7133);
#5770=PLANE('',#7134);
#5771=PLANE('',#7135);
#5772=PLANE('',#7136);
#5773=PLANE('',#7138);
#5774=PLANE('',#7146);
#6068=ADVANCED_FACE('',(#1268),#5764,.F.);
#6069=ADVANCED_FACE('',(#1269),#5765,.F.);
#6070=ADVANCED_FACE('',(#1270),#5766,.F.);
#6071=ADVANCED_FACE('',(#1271),#5767,.F.);
#6072=ADVANCED_FACE('',(#1272),#5768,.F.);
#6073=ADVANCED_FACE('',(#1273),#5769,.F.);
#6074=ADVANCED_FACE('',(#1274),#5770,.F.);
#6075=ADVANCED_FACE('',(#1275),#5771,.F.);
#6076=ADVANCED_FACE('',(#1276),#5772,.F.);
#6077=ADVANCED_FACE('',(#1277),#5773,.T.);
#6078=ADVANCED_FACE('',(#1278),#366,.T.);
#6079=ADVANCED_FACE('',(#1279),#1001,.T.);
#6080=ADVANCED_FACE('',(#1280),#367,.T.);
#6081=ADVANCED_FACE('',(#1281,#640),#5774,.T.);
#6082=ADVANCED_FACE('',(#1282),#368,.T.);
#6083=ADVANCED_FACE('',(#1283),#1002,.T.);
#6232=CLOSED_SHELL('',(#6068,#6069,#6070,#6071,#6072,#6073,#6074,#6075));
#6233=CLOSED_SHELL('',(#6076,#6077,#6078,#6079,#6080,#6081,#6082,#6083));
#7127=AXIS2_PLACEMENT_3D('',#10557,#8638,#8639);
#7128=AXIS2_PLACEMENT_3D('',#10558,#8640,#8641);
#7129=AXIS2_PLACEMENT_3D('',#10567,#8646,#8647);
#7130=AXIS2_PLACEMENT_3D('',#10573,#8651,#8652);
#7131=AXIS2_PLACEMENT_3D('',#10579,#8656,#8657);
#7132=AXIS2_PLACEMENT_3D('',#10585,#8661,#8662);
#7133=AXIS2_PLACEMENT_3D('',#10591,#8666,#8667);
#7134=AXIS2_PLACEMENT_3D('',#10594,#8670,#8671);
#7135=AXIS2_PLACEMENT_3D('',#10595,#8672,#8673);
#7136=AXIS2_PLACEMENT_3D('',#10596,#8674,#8675);
#7137=AXIS2_PLACEMENT_3D('',#10598,#8676,#8677);
#7138=AXIS2_PLACEMENT_3D('',#10599,#8678,#8679);
#7139=AXIS2_PLACEMENT_3D('',#10601,#8680,#8681);
#7140=AXIS2_PLACEMENT_3D('',#10602,#8682,#8683);
#7141=AXIS2_PLACEMENT_3D('',#10604,#8684,#8685);
#7142=AXIS2_PLACEMENT_3D('',#10606,#8687,#8688);
#7143=AXIS2_PLACEMENT_3D('',#10608,#8689,#8690);
#7144=AXIS2_PLACEMENT_3D('',#10610,#8692,#8693);
#7145=AXIS2_PLACEMENT_3D('',#10612,#8694,#8695);
#7146=AXIS2_PLACEMENT_3D('',#10614,#8697,#8698);
#7147=AXIS2_PLACEMENT_3D('',#10616,#8699,#8700);
#7148=AXIS2_PLACEMENT_3D('',#10617,#8701,#8702);
#7149=AXIS2_PLACEMENT_3D('',#10619,#8703,#8704);
#7150=AXIS2_PLACEMENT_3D('',#10621,#8706,#8707);
#8638=DIRECTION('axis',(0.,0.,1.));
#8639=DIRECTION('refdir',(1.,0.,0.));
#8640=DIRECTION('center_axis',(0.866025403784439,0.,-0.5));
#8641=DIRECTION('ref_axis',(0.5,0.,0.866025403784439));
#8642=DIRECTION('',(-0.5,0.,-0.866025403784439));
#8643=DIRECTION('',(0.,-1.,0.));
#8644=DIRECTION('',(0.5,0.,0.866025403784439));
#8645=DIRECTION('',(0.,-1.,0.));
#8646=DIRECTION('center_axis',(1.20185167898973E-16,0.,-1.));
#8647=DIRECTION('ref_axis',(1.,0.,1.20185167898973E-16));
#8648=DIRECTION('',(-1.,0.,-1.20185167898973E-16));
#8649=DIRECTION('',(0.,-1.,0.));
#8650=DIRECTION('',(1.,0.,1.20185167898973E-16));
#8651=DIRECTION('center_axis',(-0.866025403784439,0.,-0.5));
#8652=DIRECTION('ref_axis',(0.5,0.,-0.866025403784439));
#8653=DIRECTION('',(-0.5,0.,0.866025403784439));
#8654=DIRECTION('',(0.,-1.,0.));
#8655=DIRECTION('',(0.5,0.,-0.866025403784439));
#8656=DIRECTION('center_axis',(-0.866025403784439,0.,0.5));
#8657=DIRECTION('ref_axis',(-0.5,0.,-0.866025403784439));
#8658=DIRECTION('',(0.5,0.,0.866025403784439));
#8659=DIRECTION('',(0.,-1.,0.));
#8660=DIRECTION('',(-0.5,0.,-0.866025403784439));
#8661=DIRECTION('center_axis',(-2.40370335797945E-16,0.,1.));
#8662=DIRECTION('ref_axis',(-1.,0.,-2.40370335797945E-16));
#8663=DIRECTION('',(1.,0.,2.40370335797945E-16));
#8664=DIRECTION('',(0.,-1.,0.));
#8665=DIRECTION('',(-1.,0.,-2.40370335797945E-16));
#8666=DIRECTION('center_axis',(0.866025403784439,0.,0.5));
#8667=DIRECTION('ref_axis',(-0.5,0.,0.866025403784439));
#8668=DIRECTION('',(0.5,0.,-0.866025403784439));
#8669=DIRECTION('',(-0.5,0.,0.866025403784439));
#8670=DIRECTION('center_axis',(0.,1.,0.));
#8671=DIRECTION('ref_axis',(1.,0.,0.));
#8672=DIRECTION('center_axis',(0.,-1.,0.));
#8673=DIRECTION('ref_axis',(0.,0.,-1.));
#8674=DIRECTION('center_axis',(0.,1.,0.));
#8675=DIRECTION('ref_axis',(1.,0.,0.));
#8676=DIRECTION('center_axis',(0.,1.,0.));
#8677=DIRECTION('ref_axis',(1.,0.,0.));
#8678=DIRECTION('center_axis',(0.,1.,0.));
#8679=DIRECTION('ref_axis',(0.,0.,1.));
#8680=DIRECTION('center_axis',(0.,-1.,0.));
#8681=DIRECTION('ref_axis',(1.,0.,0.));
#8682=DIRECTION('center_axis',(0.,-1.,0.));
#8683=DIRECTION('ref_axis',(1.,0.,0.));
#8684=DIRECTION('center_axis',(0.,-1.,0.));
#8685=DIRECTION('ref_axis',(1.,0.,0.));
#8686=DIRECTION('',(0.707106781186548,0.707106781186547,8.65956056235493E-17));
#8687=DIRECTION('center_axis',(0.,-1.,0.));
#8688=DIRECTION('ref_axis',(1.,0.,0.));
#8689=DIRECTION('center_axis',(0.,-1.,0.));
#8690=DIRECTION('ref_axis',(1.,0.,0.));
#8691=DIRECTION('',(0.,1.,0.));
#8692=DIRECTION('center_axis',(0.,1.,0.));
#8693=DIRECTION('ref_axis',(1.,0.,0.));
#8694=DIRECTION('center_axis',(0.,-1.,0.));
#8695=DIRECTION('ref_axis',(1.,0.,0.));
#8696=DIRECTION('',(-0.707106781186547,0.707106781186548,-8.65956056235493E-17));
#8697=DIRECTION('center_axis',(0.,-1.,0.));
#8698=DIRECTION('ref_axis',(0.,0.,-1.));
#8699=DIRECTION('center_axis',(0.,-1.,0.));
#8700=DIRECTION('ref_axis',(1.,0.,0.));
#8701=DIRECTION('center_axis',(0.,1.,0.));
#8702=DIRECTION('ref_axis',(1.,0.,0.));
#8703=DIRECTION('center_axis',(0.,1.,0.));
#8704=DIRECTION('ref_axis',(1.,0.,0.));
#8705=DIRECTION('',(-0.447213595499958,0.894427190999916,-5.47678698264203E-17));
#8706=DIRECTION('center_axis',(0.,-1.,0.));
#8707=DIRECTION('ref_axis',(1.,0.,0.));
#8708=DIRECTION('',(0.,1.,0.));
#10557=CARTESIAN_POINT('',(0.,0.,0.));
#10558=CARTESIAN_POINT('Origin',(0.115470053837925,-0.5,-0.2));
#10559=CARTESIAN_POINT('',(0.23094010767585,-0.5,0.));
#10560=CARTESIAN_POINT('',(0.115470053837925,-0.5,-0.2));
#10561=CARTESIAN_POINT('',(0.23094010767585,-0.5,0.));
#10562=CARTESIAN_POINT('',(0.115470053837925,-0.8,-0.2));
#10563=CARTESIAN_POINT('',(0.115470053837925,-0.5,-0.2));
#10564=CARTESIAN_POINT('',(0.23094010767585,-0.8,0.));
#10565=CARTESIAN_POINT('',(0.23094010767585,-0.8,0.));
#10566=CARTESIAN_POINT('',(0.23094010767585,-0.5,0.));
#10567=CARTESIAN_POINT('Origin',(-0.115470053837925,-0.5,-0.2));
#10568=CARTESIAN_POINT('',(-0.115470053837925,-0.5,-0.2));
#10569=CARTESIAN_POINT('',(0.115470053837925,-0.5,-0.2));
#10570=CARTESIAN_POINT('',(-0.115470053837925,-0.8,-0.2));
#10571=CARTESIAN_POINT('',(-0.115470053837925,-0.5,-0.2));
#10572=CARTESIAN_POINT('',(0.115470053837925,-0.8,-0.2));
#10573=CARTESIAN_POINT('Origin',(-0.23094010767585,-0.5,-2.77555756156289E-17));
#10574=CARTESIAN_POINT('',(-0.23094010767585,-0.5,-2.82820063659975E-17));
#10575=CARTESIAN_POINT('',(-0.115470053837925,-0.5,-0.2));
#10576=CARTESIAN_POINT('',(-0.23094010767585,-0.8,-2.77555756156289E-17));
#10577=CARTESIAN_POINT('',(-0.23094010767585,-0.5,-2.82820063659975E-17));
#10578=CARTESIAN_POINT('',(-0.115470053837925,-0.8,-0.2));
#10579=CARTESIAN_POINT('Origin',(-0.115470053837925,-0.5,0.2));
#10580=CARTESIAN_POINT('',(-0.115470053837925,-0.5,0.2));
#10581=CARTESIAN_POINT('',(-0.23094010767585,-0.5,-2.82820063659975E-17));
#10582=CARTESIAN_POINT('',(-0.115470053837925,-0.8,0.2));
#10583=CARTESIAN_POINT('',(-0.115470053837925,-0.5,0.2));
#10584=CARTESIAN_POINT('',(-0.23094010767585,-0.8,-2.82820063659975E-17));
#10585=CARTESIAN_POINT('Origin',(0.115470053837925,-0.5,0.2));
#10586=CARTESIAN_POINT('',(0.115470053837925,-0.5,0.2));
#10587=CARTESIAN_POINT('',(-0.115470053837925,-0.5,0.2));
#10588=CARTESIAN_POINT('',(0.115470053837925,-0.8,0.2));
#10589=CARTESIAN_POINT('',(0.115470053837925,-0.5,0.2));
#10590=CARTESIAN_POINT('',(-0.115470053837925,-0.8,0.2));
#10591=CARTESIAN_POINT('Origin',(0.23094010767585,-0.5,0.));
#10592=CARTESIAN_POINT('',(0.115470053837925,-0.5,0.2));
#10593=CARTESIAN_POINT('',(0.115470053837925,-0.8,0.2));
#10594=CARTESIAN_POINT('Origin',(0.,-0.5,0.));
#10595=CARTESIAN_POINT('Origin',(0.,-0.8,0.));
#10596=CARTESIAN_POINT('Origin',(0.,-1.4,0.));
#10597=CARTESIAN_POINT('',(-0.24505,-1.4,3.00099698131059E-17));
#10598=CARTESIAN_POINT('Origin',(0.,-1.4,0.));
#10599=CARTESIAN_POINT('Origin',(0.375,0.5,0.));
#10600=CARTESIAN_POINT('',(-0.375,0.5,-4.59242549680257E-17));
#10601=CARTESIAN_POINT('Origin',(0.,0.5,0.));
#10602=CARTESIAN_POINT('Origin',(0.,0.475,0.));
#10603=CARTESIAN_POINT('',(-0.425,0.45,-5.20474889637625E-17));
#10604=CARTESIAN_POINT('Origin',(0.,0.45,0.));
#10605=CARTESIAN_POINT('',(-0.4,0.475,-4.89858719658941E-17));
#10606=CARTESIAN_POINT('Origin',(0.,0.24,0.));
#10607=CARTESIAN_POINT('',(-0.425,0.0299999999999998,-5.20474889637625E-17));
#10608=CARTESIAN_POINT('Origin',(0.,0.0299999999999998,0.));
#10609=CARTESIAN_POINT('',(-0.425,0.24,-5.20474889637625E-17));
#10610=CARTESIAN_POINT('Origin',(0.,0.0150000000000001,0.));
#10611=CARTESIAN_POINT('',(-0.395,4.85722573273506E-17,-4.83735485663204E-17));
#10612=CARTESIAN_POINT('Origin',(0.,0.,0.));
#10613=CARTESIAN_POINT('',(-0.41,0.0150000000000001,-5.02105187650415E-17));
#10614=CARTESIAN_POINT('Origin',(0.27,0.,0.));
#10615=CARTESIAN_POINT('',(-0.27,0.,-3.30654635769785E-17));
#10616=CARTESIAN_POINT('Origin',(0.,0.,0.));
#10617=CARTESIAN_POINT('Origin',(0.,-0.02,0.));
#10618=CARTESIAN_POINT('',(-0.24505,-0.0498999999999999,3.00099698131059E-17));
#10619=CARTESIAN_POINT('Origin',(0.,-0.0498999999999999,0.));
#10620=CARTESIAN_POINT('',(-0.26,-0.02,-3.18408167778312E-17));
#10621=CARTESIAN_POINT('Origin',(0.,-0.995,0.));
#10622=CARTESIAN_POINT('',(-0.24505,-0.995,-3.00099698131059E-17));
#11677=UNCERTAINTY_MEASURE_WITH_UNIT(LENGTH_MEASURE(0.001),#11749,
'DISTANCE_ACCURACY_VALUE',
'Maximum model space distance between geometric entities at asserted c
onnectivities');
#11699=UNCERTAINTY_MEASURE_WITH_UNIT(LENGTH_MEASURE(0.001),#11749,
'DISTANCE_ACCURACY_VALUE',
'Maximum model space distance between geometric entities at asserted c
onnectivities');
#11726=(
GEOMETRIC_REPRESENTATION_CONTEXT(3)
GLOBAL_UNCERTAINTY_ASSIGNED_CONTEXT((#11677))
GLOBAL_UNIT_ASSIGNED_CONTEXT((#11749,#11751,#11752))
REPRESENTATION_CONTEXT('','3D')
);
#11748=(
GEOMETRIC_REPRESENTATION_CONTEXT(3)
GLOBAL_UNCERTAINTY_ASSIGNED_CONTEXT((#11699))
GLOBAL_UNIT_ASSIGNED_CONTEXT((#11749,#11751,#11752))
REPRESENTATION_CONTEXT('','3D')
);
#11749=(
LENGTH_UNIT()
NAMED_UNIT(*)
SI_UNIT(.CENTI.,.METRE.)
);
#11751=(
NAMED_UNIT(*)
PLANE_ANGLE_UNIT()
SI_UNIT($,.RADIAN.)
);
#11752=(
NAMED_UNIT(*)
SI_UNIT($,.STERADIAN.)
SOLID_ANGLE_UNIT()
);
#11779=SHAPE_DEFINITION_REPRESENTATION(#11827,#11950);
#11827=PRODUCT_DEFINITION_SHAPE('',$,#11999);
#11950=SHAPE_REPRESENTATION('',(#7127),#11726);
#11972=PRODUCT_DEFINITION_CONTEXT('part definition',#12118,'design');
#11999=PRODUCT_DEFINITION('M5x14 Cap Screw','M5x14 Cap Screw',#12047,#11972);
#12047=PRODUCT_DEFINITION_FORMATION('',$,#12146);
#12118=APPLICATION_CONTEXT(
'Core Data for Automotive Mechanical Design Process');
#12119=PRODUCT_CONTEXT('part definition',#12118,'mechanical');
#12146=PRODUCT('M5x14 Cap Screw','M5x14 Cap Screw','M5x14 Cap Screw',(#12119));
#12172=PRESENTATION_STYLE_ASSIGNMENT((#12177));
#12177=SURFACE_STYLE_USAGE(.BOTH.,#12182);
#12182=SURFACE_SIDE_STYLE('',(#12187));
#12187=SURFACE_STYLE_FILL_AREA(#12192);
#12192=FILL_AREA_STYLE('CAD Library Painted - Graphite',(#12197));
#12197=FILL_AREA_STYLE_COLOUR('CAD Library Painted - Graphite',#12202);
#12202=COLOUR_RGB('CAD Library Painted - Graphite',0.168627450980392,0.192156862745098,
0.231372549019608);
ENDSEC;
END-ISO-10303-21;
